ISO-10303-21;
HEADER;
/* Generated by software containing ST-Developer
 * from STEP Tools, Inc. (www.steptools.com) 
 */

FILE_DESCRIPTION(
/* description */ ('Line shaft on three pillow blocks'),
/* implementation_level */ '2;1');

FILE_NAME(
/* name */ 'Drive hub (1).step',
/* time_stamp */ '2026-10-27T10:49:19-07:00',
/* author */ (''),
/* organization */ (''),
/* preprocessor_version */ 'ST-DEVELOPER v20.2',
/* originating_system */ 'Autodesk Translation Framework v15.17.0.0',
/* authorisation */ '');

FILE_SCHEMA (('AUTOMOTIVE_DESIGN { 1 0 10303 214 3 1 1 }'));
ENDSEC;

DATA;
#10=MECHANICAL_DESIGN_GEOMETRIC_PRESENTATION_REPRESENTATION('',(#358),#8377);
#251=B_SPLINE_CURVE_WITH_KNOTS('',3,(#7805,#7806,#7807,#7808,#7809,#7810,
#7811,#7812,#7813,#7814),.UNSPECIFIED.,.F.,.F.,(4,2,2,2,4),(0.803821788694082,
0.872950991853617,0.952307212900967,1.03166343394832,1.10079263710785),
 .UNSPECIFIED.);
#252=B_SPLINE_CURVE_WITH_KNOTS('',3,(#7820,#7821,#7822,#7823,#7824,#7825,
#7826,#7827,#7828,#7829,#7830,#7831,#7832,#7833,#7834,#7835,#7836,#7837),
 .UNSPECIFIED.,.F.,.F.,(4,2,2,2,2,2,2,2,4),(0.,0.0791670250779298,0.15833405015586,
0.237500747381211,0.316667444606563,0.395834141831915,0.475000839057267,
0.554167864135197,0.633334889213127),.UNSPECIFIED.);
#253=B_SPLINE_CURVE_WITH_KNOTS('',3,(#7838,#7839,#7840,#7841,#7842,#7843,
#7844,#7845,#7846,#7847,#7848,#7849,#7850,#7851,#7852,#7853,#7854,#7855),
 .UNSPECIFIED.,.F.,.F.,(4,2,2,2,2,2,2,2,4),(0.633334889213127,0.712501914291057,
0.791668939368986,0.870835636594338,0.95000233381969,1.02916903104504,1.10833572827039,
1.18750275334832,1.26666977842625),.UNSPECIFIED.);
#254=B_SPLINE_CURVE_WITH_KNOTS('',3,(#7858,#7859,#7860,#7861,#7862,#7863,
#7864,#7865,#7866,#7867),.UNSPECIFIED.,.F.,.F.,(4,2,2,2,4),(0.168950313426766,
0.238079516586306,0.317435737633656,0.396791958681006,0.46592116184054),
 .UNSPECIFIED.);
#303=SHAPE_REPRESENTATION_RELATIONSHIP('SRR','None',#8520,#330);
#330=ADVANCED_BREP_SHAPE_REPRESENTATION('',(#384),#8369);
#358=STYLED_ITEM('',(#8704),#384);
#384=MANIFOLD_SOLID_BREP('Body1',#4346);
#470=FACE_BOUND('',#1173,.T.);
#471=FACE_BOUND('',#1175,.T.);
#472=FACE_BOUND('',#1177,.T.);
#473=FACE_BOUND('',#1179,.T.);
#605=PLANE('',#5012);
#606=PLANE('',#5017);
#607=PLANE('',#5018);
#608=PLANE('',#5019);
#609=PLANE('',#5020);
#610=PLANE('',#5021);
#611=PLANE('',#5028);
#835=FACE_OUTER_BOUND('',#1166,.T.);
#836=FACE_OUTER_BOUND('',#1167,.T.);
#837=FACE_OUTER_BOUND('',#1168,.T.);
#838=FACE_OUTER_BOUND('',#1169,.T.);
#839=FACE_OUTER_BOUND('',#1170,.T.);
#840=FACE_OUTER_BOUND('',#1171,.T.);
#841=FACE_OUTER_BOUND('',#1172,.T.);
#842=FACE_OUTER_BOUND('',#1174,.T.);
#843=FACE_OUTER_BOUND('',#1176,.T.);
#844=FACE_OUTER_BOUND('',#1178,.T.);
#1166=EDGE_LOOP('',(#3701,#3702));
#1167=EDGE_LOOP('',(#3703,#3704,#3705,#3706,#3707,#3708,#3709,#3710,#3711));
#1168=EDGE_LOOP('',(#3712,#3713,#3714));
#1169=EDGE_LOOP('',(#3715,#3716,#3717,#3718));
#1170=EDGE_LOOP('',(#3719,#3720,#3721,#3722));
#1171=EDGE_LOOP('',(#3723,#3724,#3725,#3726));
#1172=EDGE_LOOP('',(#3727));
#1173=EDGE_LOOP('',(#3728,#3729,#3730,#3731));
#1174=EDGE_LOOP('',(#3732,#3733,#3734,#3735));
#1175=EDGE_LOOP('',(#3736,#3737,#3738,#3739));
#1176=EDGE_LOOP('',(#3740,#3741,#3742,#3743));
#1177=EDGE_LOOP('',(#3744,#3745));
#1178=EDGE_LOOP('',(#3746));
#1179=EDGE_LOOP('',(#3747,#3748,#3749,#3750));
#1485=LINE('',#7801,#1812);
#1486=LINE('',#7818,#1813);
#1487=LINE('',#7869,#1814);
#1488=LINE('',#7873,#1815);
#1489=LINE('',#7875,#1816);
#1490=LINE('',#7877,#1817);
#1491=LINE('',#7878,#1818);
#1492=LINE('',#7881,#1819);
#1493=LINE('',#7883,#1820);
#1494=LINE('',#7884,#1821);
#1495=LINE('',#7887,#1822);
#1496=LINE('',#7889,#1823);
#1497=LINE('',#7890,#1824);
#1498=LINE('',#7899,#1825);
#1812=VECTOR('',#6098,1.);
#1813=VECTOR('',#6105,0.21);
#1814=VECTOR('',#6110,1.);
#1815=VECTOR('',#6113,1.);
#1816=VECTOR('',#6114,1.);
#1817=VECTOR('',#6115,1.);
#1818=VECTOR('',#6116,1.);
#1819=VECTOR('',#6119,1.);
#1820=VECTOR('',#6120,1.);
#1821=VECTOR('',#6121,1.);
#1822=VECTOR('',#6124,1.);
#1823=VECTOR('',#6125,1.);
#1824=VECTOR('',#6126,1.);
#1825=VECTOR('',#6139,2.);
#2027=CIRCLE('',#5013,0.21);
#2028=CIRCLE('',#5015,0.21);
#2029=CIRCLE('',#5016,0.21);
#2030=CIRCLE('',#5022,2.);
#2031=CIRCLE('',#5023,1.);
#2032=CIRCLE('',#5025,1.);
#2033=CIRCLE('',#5027,2.);
#2324=VERTEX_POINT('',#7799);
#2325=VERTEX_POINT('',#7800);
#2326=VERTEX_POINT('',#7804);
#2327=VERTEX_POINT('',#7815);
#2328=VERTEX_POINT('',#7817);
#2329=VERTEX_POINT('',#7819);
#2330=VERTEX_POINT('',#7856);
#2331=VERTEX_POINT('',#7871);
#2332=VERTEX_POINT('',#7872);
#2333=VERTEX_POINT('',#7874);
#2334=VERTEX_POINT('',#7876);
#2335=VERTEX_POINT('',#7880);
#2336=VERTEX_POINT('',#7882);
#2337=VERTEX_POINT('',#7886);
#2338=VERTEX_POINT('',#7888);
#2339=VERTEX_POINT('',#7892);
#2340=VERTEX_POINT('',#7898);
#2799=EDGE_CURVE('',#2324,#2325,#1485,.T.);
#2800=EDGE_CURVE('',#2324,#2325,#2027,.T.);
#2801=EDGE_CURVE('',#2326,#2324,#251,.T.);
#2802=EDGE_CURVE('',#2327,#2326,#2028,.T.);
#2803=EDGE_CURVE('',#2327,#2328,#1486,.T.);
#2804=EDGE_CURVE('',#2329,#2328,#252,.T.);
#2805=EDGE_CURVE('',#2328,#2329,#253,.T.);
#2806=EDGE_CURVE('',#2330,#2327,#2029,.T.);
#2807=EDGE_CURVE('',#2325,#2330,#254,.T.);
#2808=EDGE_CURVE('',#2330,#2326,#1487,.T.);
#2809=EDGE_CURVE('',#2331,#2332,#1488,.T.);
#2810=EDGE_CURVE('',#2331,#2333,#1489,.T.);
#2811=EDGE_CURVE('',#2334,#2333,#1490,.T.);
#2812=EDGE_CURVE('',#2332,#2334,#1491,.T.);
#2813=EDGE_CURVE('',#2335,#2331,#1492,.T.);
#2814=EDGE_CURVE('',#2335,#2336,#1493,.T.);
#2815=EDGE_CURVE('',#2333,#2336,#1494,.T.);
#2816=EDGE_CURVE('',#2337,#2335,#1495,.T.);
#2817=EDGE_CURVE('',#2338,#2337,#1496,.T.);
#2818=EDGE_CURVE('',#2336,#2338,#1497,.T.);
#2819=EDGE_CURVE('',#2339,#2339,#2030,.T.);
#2820=EDGE_CURVE('',#2338,#2334,#2031,.T.);
#2821=EDGE_CURVE('',#2337,#2332,#2032,.T.);
#2822=EDGE_CURVE('',#2339,#2340,#1498,.T.);
#2823=EDGE_CURVE('',#2340,#2340,#2033,.T.);
#3701=ORIENTED_EDGE('',*,*,#2799,.F.);
#3702=ORIENTED_EDGE('',*,*,#2800,.T.);
#3703=ORIENTED_EDGE('',*,*,#2801,.F.);
#3704=ORIENTED_EDGE('',*,*,#2802,.F.);
#3705=ORIENTED_EDGE('',*,*,#2803,.T.);
#3706=ORIENTED_EDGE('',*,*,#2804,.F.);
#3707=ORIENTED_EDGE('',*,*,#2805,.F.);
#3708=ORIENTED_EDGE('',*,*,#2803,.F.);
#3709=ORIENTED_EDGE('',*,*,#2806,.F.);
#3710=ORIENTED_EDGE('',*,*,#2807,.F.);
#3711=ORIENTED_EDGE('',*,*,#2800,.F.);
#3712=ORIENTED_EDGE('',*,*,#2808,.F.);
#3713=ORIENTED_EDGE('',*,*,#2806,.T.);
#3714=ORIENTED_EDGE('',*,*,#2802,.T.);
#3715=ORIENTED_EDGE('',*,*,#2809,.F.);
#3716=ORIENTED_EDGE('',*,*,#2810,.T.);
#3717=ORIENTED_EDGE('',*,*,#2811,.F.);
#3718=ORIENTED_EDGE('',*,*,#2812,.F.);
#3719=ORIENTED_EDGE('',*,*,#2813,.F.);
#3720=ORIENTED_EDGE('',*,*,#2814,.T.);
#3721=ORIENTED_EDGE('',*,*,#2815,.F.);
#3722=ORIENTED_EDGE('',*,*,#2810,.F.);
#3723=ORIENTED_EDGE('',*,*,#2816,.F.);
#3724=ORIENTED_EDGE('',*,*,#2817,.F.);
#3725=ORIENTED_EDGE('',*,*,#2818,.F.);
#3726=ORIENTED_EDGE('',*,*,#2814,.F.);
#3727=ORIENTED_EDGE('',*,*,#2819,.T.);
#3728=ORIENTED_EDGE('',*,*,#2811,.T.);
#3729=ORIENTED_EDGE('',*,*,#2815,.T.);
#3730=ORIENTED_EDGE('',*,*,#2818,.T.);
#3731=ORIENTED_EDGE('',*,*,#2820,.T.);
#3732=ORIENTED_EDGE('',*,*,#2812,.T.);
#3733=ORIENTED_EDGE('',*,*,#2820,.F.);
#3734=ORIENTED_EDGE('',*,*,#2817,.T.);
#3735=ORIENTED_EDGE('',*,*,#2821,.T.);
#3736=ORIENTED_EDGE('',*,*,#2807,.T.);
#3737=ORIENTED_EDGE('',*,*,#2808,.T.);
#3738=ORIENTED_EDGE('',*,*,#2801,.T.);
#3739=ORIENTED_EDGE('',*,*,#2799,.T.);
#3740=ORIENTED_EDGE('',*,*,#2819,.F.);
#3741=ORIENTED_EDGE('',*,*,#2822,.T.);
#3742=ORIENTED_EDGE('',*,*,#2823,.T.);
#3743=ORIENTED_EDGE('',*,*,#2822,.F.);
#3744=ORIENTED_EDGE('',*,*,#2804,.T.);
#3745=ORIENTED_EDGE('',*,*,#2805,.T.);
#3746=ORIENTED_EDGE('',*,*,#2823,.F.);
#3747=ORIENTED_EDGE('',*,*,#2809,.T.);
#3748=ORIENTED_EDGE('',*,*,#2821,.F.);
#3749=ORIENTED_EDGE('',*,*,#2816,.T.);
#3750=ORIENTED_EDGE('',*,*,#2813,.T.);
#4056=CYLINDRICAL_SURFACE('',#5014,0.21);
#4057=CYLINDRICAL_SURFACE('',#5024,1.);
#4058=CYLINDRICAL_SURFACE('',#5026,2.);
#4253=ADVANCED_FACE('',(#835),#605,.T.);
#4254=ADVANCED_FACE('',(#836),#4056,.F.);
#4255=ADVANCED_FACE('',(#837),#606,.T.);
#4256=ADVANCED_FACE('',(#838),#607,.F.);
#4257=ADVANCED_FACE('',(#839),#608,.F.);
#4258=ADVANCED_FACE('',(#840),#609,.F.);
#4259=ADVANCED_FACE('',(#841,#470),#610,.T.);
#4260=ADVANCED_FACE('',(#842,#471),#4057,.F.);
#4261=ADVANCED_FACE('',(#843,#472),#4058,.T.);
#4262=ADVANCED_FACE('',(#844,#473),#611,.F.);
#4346=CLOSED_SHELL('',(#4253,#4254,#4255,#4256,#4257,#4258,#4259,#4260,
#4261,#4262));
#5011=AXIS2_PLACEMENT_3D('',#7797,#6094,#6095);
#5012=AXIS2_PLACEMENT_3D('',#7798,#6096,#6097);
#5013=AXIS2_PLACEMENT_3D('',#7802,#6099,#6100);
#5014=AXIS2_PLACEMENT_3D('',#7803,#6101,#6102);
#5015=AXIS2_PLACEMENT_3D('',#7816,#6103,#6104);
#5016=AXIS2_PLACEMENT_3D('',#7857,#6106,#6107);
#5017=AXIS2_PLACEMENT_3D('',#7868,#6108,#6109);
#5018=AXIS2_PLACEMENT_3D('',#7870,#6111,#6112);
#5019=AXIS2_PLACEMENT_3D('',#7879,#6117,#6118);
#5020=AXIS2_PLACEMENT_3D('',#7885,#6122,#6123);
#5021=AXIS2_PLACEMENT_3D('',#7891,#6127,#6128);
#5022=AXIS2_PLACEMENT_3D('',#7893,#6129,#6130);
#5023=AXIS2_PLACEMENT_3D('',#7894,#6131,#6132);
#5024=AXIS2_PLACEMENT_3D('',#7895,#6133,#6134);
#5025=AXIS2_PLACEMENT_3D('',#7896,#6135,#6136);
#5026=AXIS2_PLACEMENT_3D('',#7897,#6137,#6138);
#5027=AXIS2_PLACEMENT_3D('',#7900,#6140,#6141);
#5028=AXIS2_PLACEMENT_3D('',#7901,#6142,#6143);
#6094=DIRECTION('axis',(0.,0.,1.));
#6095=DIRECTION('refdir',(1.,0.,0.));
#6096=DIRECTION('center_axis',(0.,0.,1.));
#6097=DIRECTION('ref_axis',(1.,0.,0.));
#6098=DIRECTION('',(0.,1.,0.));
#6099=DIRECTION('center_axis',(0.,0.,1.));
#6100=DIRECTION('ref_axis',(1.,0.,0.));
#6101=DIRECTION('center_axis',(0.,0.,1.));
#6102=DIRECTION('ref_axis',(1.,0.,0.));
#6103=DIRECTION('center_axis',(0.,0.,1.));
#6104=DIRECTION('ref_axis',(1.,0.,0.));
#6105=DIRECTION('',(0.,0.,1.));
#6106=DIRECTION('center_axis',(0.,0.,1.));
#6107=DIRECTION('ref_axis',(1.,0.,0.));
#6108=DIRECTION('center_axis',(0.,0.,1.));
#6109=DIRECTION('ref_axis',(1.,0.,0.));
#6110=DIRECTION('',(0.,-1.,0.));
#6111=DIRECTION('center_axis',(-1.,0.,0.));
#6112=DIRECTION('ref_axis',(0.,0.,1.));
#6113=DIRECTION('',(0.,0.,1.));
#6114=DIRECTION('',(0.,1.,0.));
#6115=DIRECTION('',(0.,0.,-1.));
#6116=DIRECTION('',(0.,1.,0.));
#6117=DIRECTION('center_axis',(0.,0.,-1.));
#6118=DIRECTION('ref_axis',(-1.,0.,0.));
#6119=DIRECTION('',(-1.,0.,0.));
#6120=DIRECTION('',(0.,1.,0.));
#6121=DIRECTION('',(1.,0.,0.));
#6122=DIRECTION('center_axis',(1.,0.,0.));
#6123=DIRECTION('ref_axis',(0.,0.,-1.));
#6124=DIRECTION('',(0.,0.,-1.));
#6125=DIRECTION('',(0.,-1.,0.));
#6126=DIRECTION('',(0.,0.,1.));
#6127=DIRECTION('center_axis',(0.,1.,0.));
#6128=DIRECTION('ref_axis',(1.,0.,0.));
#6129=DIRECTION('center_axis',(0.,1.,0.));
#6130=DIRECTION('ref_axis',(1.,0.,0.));
#6131=DIRECTION('center_axis',(0.,-1.,0.));
#6132=DIRECTION('ref_axis',(1.,0.,0.));
#6133=DIRECTION('center_axis',(0.,1.,0.));
#6134=DIRECTION('ref_axis',(-1.83697019872103E-16,0.,1.));
#6135=DIRECTION('center_axis',(0.,-1.,0.));
#6136=DIRECTION('ref_axis',(1.,0.,0.));
#6137=DIRECTION('center_axis',(0.,1.,0.));
#6138=DIRECTION('ref_axis',(1.,0.,0.));
#6139=DIRECTION('',(0.,-1.,0.));
#6140=DIRECTION('center_axis',(0.,1.,0.));
#6141=DIRECTION('ref_axis',(1.,0.,0.));
#6142=DIRECTION('center_axis',(0.,1.,0.));
#6143=DIRECTION('ref_axis',(1.,0.,0.));
#7797=CARTESIAN_POINT('',(0.,0.,0.));
#7798=CARTESIAN_POINT('Origin',(0.,22.25,5.52));
#7799=CARTESIAN_POINT('',(0.141067359796651,22.094436508139,5.52));
#7800=CARTESIAN_POINT('',(0.141067359796651,22.405563491861,5.52));
#7801=CARTESIAN_POINT('',(0.141067359796651,21.,5.52));
#7802=CARTESIAN_POINT('Origin',(0.,22.25,5.52));
#7803=CARTESIAN_POINT('Origin',(0.,22.25,5.52));
#7804=CARTESIAN_POINT('',(-0.141067359796651,22.094436508139,5.52));
#7805=CARTESIAN_POINT('Ctrl Pts',(-0.141067359796651,22.094436508139,5.52));
#7806=CARTESIAN_POINT('Ctrl Pts',(-0.123818356698221,22.0787948476368,5.52245784982447));
#7807=CARTESIAN_POINT('Ctrl Pts',(-0.102998643109697,22.065375956669,5.52493819304946));
#7808=CARTESIAN_POINT('Ctrl Pts',(-0.0546141143983537,22.0453025362756,
5.52884449237241));
#7809=CARTESIAN_POINT('Ctrl Pts',(-0.02645207368245,22.04,5.53));
#7810=CARTESIAN_POINT('Ctrl Pts',(0.02645207368245,22.04,5.53));
#7811=CARTESIAN_POINT('Ctrl Pts',(0.0546141143983536,22.0453025362756,5.52884449237241));
#7812=CARTESIAN_POINT('Ctrl Pts',(0.102998643109697,22.065375956669,5.52493819304946));
#7813=CARTESIAN_POINT('Ctrl Pts',(0.123818356698218,22.0787948476368,5.52245784982447));
#7814=CARTESIAN_POINT('Ctrl Pts',(0.141067359796651,22.094436508139,5.52));
#7815=CARTESIAN_POINT('',(-0.21,22.25,5.52));
#7816=CARTESIAN_POINT('Origin',(0.,22.25,5.52));
#7817=CARTESIAN_POINT('',(-0.21,22.25,6.51894444366855));
#7818=CARTESIAN_POINT('',(-0.21,22.25,5.52));
#7819=CARTESIAN_POINT('',(0.21,22.25,6.51894444366855));
#7820=CARTESIAN_POINT('Ctrl Pts',(0.21,22.25,6.51894444366855));
#7821=CARTESIAN_POINT('Ctrl Pts',(0.21,22.2236109916407,6.51894444366855));
#7822=CARTESIAN_POINT('Ctrl Pts',(0.204722164681422,22.1954764062218,6.51952376620524));
#7823=CARTESIAN_POINT('Ctrl Pts',(0.18328486745047,22.1437425531788,6.52161307432363));
#7824=CARTESIAN_POINT('Ctrl Pts',(0.167126466290583,22.1201416181922,6.52309254589373));
#7825=CARTESIAN_POINT('Ctrl Pts',(0.129858458976496,22.0828736108781,6.52586721250997));
#7826=CARTESIAN_POINT('Ctrl Pts',(0.106257490219277,22.0667151494345,6.527343117591));
#7827=CARTESIAN_POINT('Ctrl Pts',(0.0545235237847864,22.0452778074131,6.52942425936951));
#7828=CARTESIAN_POINT('Ctrl Pts',(0.0263888990751173,22.04,6.53));
#7829=CARTESIAN_POINT('Ctrl Pts',(-0.0263888990751173,22.04,6.53));
#7830=CARTESIAN_POINT('Ctrl Pts',(-0.0545235237847876,22.0452778074131,
6.52942425936951));
#7831=CARTESIAN_POINT('Ctrl Pts',(-0.106257490219279,22.0667151494345,6.527343117591));
#7832=CARTESIAN_POINT('Ctrl Pts',(-0.129858458976496,22.0828736108781,6.52586721250997));
#7833=CARTESIAN_POINT('Ctrl Pts',(-0.167126466290583,22.1201416181922,6.52309254589373));
#7834=CARTESIAN_POINT('Ctrl Pts',(-0.18328486745047,22.1437425531788,6.52161307432363));
#7835=CARTESIAN_POINT('Ctrl Pts',(-0.204722164681422,22.1954764062218,6.51952376620524));
#7836=CARTESIAN_POINT('Ctrl Pts',(-0.21,22.2236109916407,6.51894444366855));
#7837=CARTESIAN_POINT('Ctrl Pts',(-0.21,22.25,6.51894444366855));
#7838=CARTESIAN_POINT('Ctrl Pts',(-0.21,22.25,6.51894444366855));
#7839=CARTESIAN_POINT('Ctrl Pts',(-0.21,22.2763890083593,6.51894444366855));
#7840=CARTESIAN_POINT('Ctrl Pts',(-0.204722164681422,22.3045235937782,6.51952376620524));
#7841=CARTESIAN_POINT('Ctrl Pts',(-0.18328486745047,22.3562574468212,6.52161307432363));
#7842=CARTESIAN_POINT('Ctrl Pts',(-0.167126466290583,22.3798583818078,6.52309254589373));
#7843=CARTESIAN_POINT('Ctrl Pts',(-0.129858458976496,22.4171263891219,6.52586721250997));
#7844=CARTESIAN_POINT('Ctrl Pts',(-0.106257490219277,22.4332848505655,6.527343117591));
#7845=CARTESIAN_POINT('Ctrl Pts',(-0.0545235237847864,22.4547221925869,
6.52942425936951));
#7846=CARTESIAN_POINT('Ctrl Pts',(-0.0263888990751173,22.46,6.53));
#7847=CARTESIAN_POINT('Ctrl Pts',(0.0263888990751173,22.46,6.53));
#7848=CARTESIAN_POINT('Ctrl Pts',(0.054523523784789,22.4547221925869,6.52942425936951));
#7849=CARTESIAN_POINT('Ctrl Pts',(0.106257490219279,22.4332848505655,6.527343117591));
#7850=CARTESIAN_POINT('Ctrl Pts',(0.129858458976496,22.4171263891219,6.52586721250997));
#7851=CARTESIAN_POINT('Ctrl Pts',(0.167126466290583,22.3798583818078,6.52309254589373));
#7852=CARTESIAN_POINT('Ctrl Pts',(0.183284867450474,22.3562574468211,6.52161307432363));
#7853=CARTESIAN_POINT('Ctrl Pts',(0.204722164681421,22.3045235937782,6.51952376620524));
#7854=CARTESIAN_POINT('Ctrl Pts',(0.21,22.2763890083593,6.51894444366855));
#7855=CARTESIAN_POINT('Ctrl Pts',(0.21,22.25,6.51894444366855));
#7856=CARTESIAN_POINT('',(-0.141067359796651,22.405563491861,5.52));
#7857=CARTESIAN_POINT('Origin',(0.,22.25,5.52));
#7858=CARTESIAN_POINT('Ctrl Pts',(0.141067359796648,22.405563491861,5.52));
#7859=CARTESIAN_POINT('Ctrl Pts',(0.123818356698219,22.4212051523632,5.52245784982446));
#7860=CARTESIAN_POINT('Ctrl Pts',(0.102998643109699,22.434624043331,5.52493819304946));
#7861=CARTESIAN_POINT('Ctrl Pts',(0.0546141143983536,22.4546974637244,5.52884449237241));
#7862=CARTESIAN_POINT('Ctrl Pts',(0.02645207368245,22.46,5.53));
#7863=CARTESIAN_POINT('Ctrl Pts',(-0.02645207368245,22.46,5.53));
#7864=CARTESIAN_POINT('Ctrl Pts',(-0.0546141143983536,22.4546974637244,
5.52884449237241));
#7865=CARTESIAN_POINT('Ctrl Pts',(-0.102998643109697,22.434624043331,5.52493819304946));
#7866=CARTESIAN_POINT('Ctrl Pts',(-0.123818356698221,22.4212051523632,5.52245784982446));
#7867=CARTESIAN_POINT('Ctrl Pts',(-0.141067359796651,22.405563491861,5.52));
#7868=CARTESIAN_POINT('Origin',(0.,22.25,5.52));
#7869=CARTESIAN_POINT('',(-0.141067359796651,21.,5.52));
#7870=CARTESIAN_POINT('Origin',(-0.3,20.9,3.25));
#7871=CARTESIAN_POINT('',(-0.3,21.,3.25));
#7872=CARTESIAN_POINT('',(-0.3,21.,3.57606079858305));
#7873=CARTESIAN_POINT('',(-0.3,21.,3.89));
#7874=CARTESIAN_POINT('',(-0.3,23.5,3.25));
#7875=CARTESIAN_POINT('',(-0.3,20.9,3.25));
#7876=CARTESIAN_POINT('',(-0.3,23.5,3.57606079858305));
#7877=CARTESIAN_POINT('',(-0.3,23.5,3.89));
#7878=CARTESIAN_POINT('',(-0.3,21.,3.57606079858305));
#7879=CARTESIAN_POINT('Origin',(0.3,20.9,3.25));
#7880=CARTESIAN_POINT('',(0.3,21.,3.25));
#7881=CARTESIAN_POINT('',(0.15,21.,3.25));
#7882=CARTESIAN_POINT('',(0.3,23.5,3.25));
#7883=CARTESIAN_POINT('',(0.3,20.9,3.25));
#7884=CARTESIAN_POINT('',(0.15,23.5,3.25));
#7885=CARTESIAN_POINT('Origin',(0.3,20.9,4.53));
#7886=CARTESIAN_POINT('',(0.3,21.,3.57606079858305));
#7887=CARTESIAN_POINT('',(0.3,21.,4.53));
#7888=CARTESIAN_POINT('',(0.3,23.5,3.57606079858305));
#7889=CARTESIAN_POINT('',(0.3,21.,3.57606079858305));
#7890=CARTESIAN_POINT('',(0.3,23.5,4.53));
#7891=CARTESIAN_POINT('Origin',(0.,23.5,4.53));
#7892=CARTESIAN_POINT('',(-2.,23.5,4.53));
#7893=CARTESIAN_POINT('Origin',(0.,23.5,4.53));
#7894=CARTESIAN_POINT('Origin',(0.,23.5,4.53));
#7895=CARTESIAN_POINT('Origin',(0.,21.,4.53));
#7896=CARTESIAN_POINT('Origin',(0.,21.,4.53));
#7897=CARTESIAN_POINT('Origin',(0.,21.,4.53));
#7898=CARTESIAN_POINT('',(-2.,21.,4.53));
#7899=CARTESIAN_POINT('',(-2.,21.,4.53));
#7900=CARTESIAN_POINT('Origin',(0.,21.,4.53));
#7901=CARTESIAN_POINT('Origin',(0.,21.,4.53));
#8337=UNCERTAINTY_MEASURE_WITH_UNIT(LENGTH_MEASURE(0.001),#8378,
'DISTANCE_ACCURACY_VALUE',
'Maximum model space distance between geometric entities at asserted c
onnectivities');
#8345=UNCERTAINTY_MEASURE_WITH_UNIT(LENGTH_MEASURE(0.001),#8378,
'DISTANCE_ACCURACY_VALUE',
'Maximum model space distance between geometric entities at asserted c
onnectivities');
#8369=(
GEOMETRIC_REPRESENTATION_CONTEXT(3)
GLOBAL_UNCERTAINTY_ASSIGNED_CONTEXT((#8337))
GLOBAL_UNIT_ASSIGNED_CONTEXT((#8378,#8380,#8381))
REPRESENTATION_CONTEXT('','3D')
);
#8377=(
GEOMETRIC_REPRESENTATION_CONTEXT(3)
GLOBAL_UNCERTAINTY_ASSIGNED_CONTEXT((#8345))
GLOBAL_UNIT_ASSIGNED_CONTEXT((#8378,#8380,#8381))
REPRESENTATION_CONTEXT('','3D')
);
#8378=(
LENGTH_UNIT()
NAMED_UNIT(*)
SI_UNIT(.CENTI.,.METRE.)
);
#8380=(
NAMED_UNIT(*)
PLANE_ANGLE_UNIT()
SI_UNIT($,.RADIAN.)
);
#8381=(
NAMED_UNIT(*)
SI_UNIT($,.STERADIAN.)
SOLID_ANGLE_UNIT()
);
#8405=SHAPE_DEFINITION_REPRESENTATION(#8472,#8520);
#8472=PRODUCT_DEFINITION_SHAPE('',$,#8552);
#8520=SHAPE_REPRESENTATION('',(#5011),#8369);
#8528=PRODUCT_DEFINITION_CONTEXT('part definition',#8623,'design');
#8552=PRODUCT_DEFINITION('Drive hub (1)','Drive hub (1)',#8583,#8528);
#8583=PRODUCT_DEFINITION_FORMATION('',$,#8648);
#8623=APPLICATION_CONTEXT(
'Core Data for Automotive Mechanical Design Process');
#8624=PRODUCT_CONTEXT('part definition',#8623,'mechanical');
#8648=PRODUCT('Drive hub (1)','Drive hub (1)','Drive hub (1)',(#8624));
#8698=COLOUR_RGB('Light Blue',0.38,0.62,0.78);
#8699=FILL_AREA_STYLE_COLOUR('',#8698);
#8700=FILL_AREA_STYLE('',(#8699));
#8701=SURFACE_STYLE_FILL_AREA(#8700);
#8702=SURFACE_SIDE_STYLE('',(#8701));
#8703=SURFACE_STYLE_USAGE(.BOTH.,#8702);
#8704=PRESENTATION_STYLE_ASSIGNMENT((#8703));
ENDSEC;
END-ISO-10303-21;
